ISO-10303-21;
HEADER;
FILE_DESCRIPTION (('STEP AP214'),
    '1' );
FILE_NAME ('Mounting Feet.step',
    '2026-10-09T16:01:55',
    ( '' ),
    ( '' ),
    'SwSTEP 2.0',
    'SolidWorks 2024',
    '' );
FILE_SCHEMA (( 'AUTOMOTIVE_DESIGN' ));
ENDSEC;

DATA;
#25=FACE_OUTER_BOUND ( 'NONE', #67171, .T. ) ;
#791=ORIENTED_EDGE ( 'NONE', *, *, #7025, .T. ) ;
#859=EDGE_CURVE ( 'NONE', #63319, #31475, #10678, .T. ) ;
#939=CARTESIAN_POINT ( 'NONE',  ( 158.8349105750994568, -35.83962462487175316, 5.000000000000000000 ) ) ;
#1327=VECTOR ( 'NONE', #17482, 1000.000000000000000 ) ;
#1484=EDGE_LOOP ( 'NONE', ( #51385, #66092, #32923, #69891 ) ) ;
#1787=CARTESIAN_POINT ( 'NONE',  ( 158.0064834503532722, -35.83962462487175316, 0.000000000000000000 ) ) ;
#1842=EDGE_CURVE ( 'NONE', #49731, #2475, #63399, .T. ) ;
#2401=AXIS2_PLACEMENT_3D ( 'NONE', #55386, #6924, #28834 ) ;
#2475=VERTEX_POINT ( 'NONE', #14875 ) ;
#2547=CARTESIAN_POINT ( 'NONE',  ( 154.0064834503532722, -29.01119750012554732, 5.000000000000000000 ) ) ;
#2573=VECTOR ( 'NONE', #8814, 1000.000000000000000 ) ;
#2579=EDGE_CURVE ( 'NONE', #43137, #34664, #26530, .T. ) ;
#2699=LINE ( 'NONE', #47256, #5416 ) ;
#2825=FACE_OUTER_BOUND ( 'NONE', #63781, .T. ) ;
#3378=VERTEX_POINT ( 'NONE', #24760 ) ;
#3572=EDGE_CURVE ( 'NONE', #7104, #67892, #25823, .T. ) ;
#4087=CIRCLE ( 'NONE', #27794, 2.000000000000001776 ) ;
#4220=VERTEX_POINT ( 'NONE', #56072 ) ;
#4271=CARTESIAN_POINT ( 'NONE',  ( 176.0064834503533575, -29.01119750012555443, 0.000000000000000000 ) ) ;
#4285=EDGE_CURVE ( 'NONE', #49731, #46063, #30863, .T. ) ;
#4625=ORIENTED_EDGE ( 'NONE', *, *, #66897, .F. ) ;
#4767=CARTESIAN_POINT ( 'NONE',  ( 158.8349105750994568, -35.83962462487175316, 0.000000000000000000 ) ) ;
#4864=ORIENTED_EDGE ( 'NONE', *, *, #24056, .T. ) ;
#5073=CARTESIAN_POINT ( 'NONE',  ( 169.1780563256071446, -35.83962462487175316, 5.000000000000000000 ) ) ;
#5416=VECTOR ( 'NONE', #62439, 1000.000000000000000 ) ;
#5677=DIRECTION ( 'NONE',  ( -1.000000000000000000, 0.000000000000000000, 0.000000000000000000 ) ) ;
#5795=LINE ( 'NONE', #22402, #64527 ) ;
#5886=AXIS2_PLACEMENT_3D ( 'NONE', #10922, #39842, #17939 ) ;
#6175=( LENGTH_UNIT ( ) NAMED_UNIT ( * ) SI_UNIT ( .MILLI., .METRE. ) );
#6191=CARTESIAN_POINT ( 'NONE',  ( 61.08342941274106153, 61.08342941274084126, 5.000000000000000000 ) ) ;
#6494=CARTESIAN_POINT ( 'NONE',  ( 154.0064834503532722, -29.01119750012554732, 5.000000000000000000 ) ) ;
#6716=EDGE_CURVE ( 'NONE', #67892, #7660, #48727, .T. ) ;
#6924=DIRECTION ( 'NONE',  ( 0.000000000000000000, -0.000000000000000000, -1.000000000000000000 ) ) ;
#6929=DIRECTION ( 'NONE',  ( 0.7071067811865487940, 0.7071067811865463515, 0.000000000000000000 ) ) ;
#7025=EDGE_CURVE ( 'NONE', #7104, #14185, #66282, .T. ) ;
#7047=VERTEX_POINT ( 'NONE', #38375 ) ;
#7092=DIRECTION ( 'NONE',  ( 0.000000000000000000, 0.000000000000000000, -1.000000000000000000 ) ) ;
#7104=VERTEX_POINT ( 'NONE', #35479 ) ;
#7185=EDGE_CURVE ( 'NONE', #63319, #7047, #7571, .T. ) ;
#7571=LINE ( 'NONE', #12855, #62289 ) ;
#7660=VERTEX_POINT ( 'NONE', #61026 ) ;
#7672=EDGE_CURVE ( 'NONE', #69051, #28084, #24800, .T. ) ;
#8060=ORIENTED_EDGE ( 'NONE', *, *, #30620, .F. ) ;
#8150=EDGE_LOOP ( 'NONE', ( #8060, #46712, #54920, #42841 ) ) ;
#8397=ORIENTED_EDGE ( 'NONE', *, *, #42332, .T. ) ;
#8597=VECTOR ( 'NONE', #66554, 1000.000000000000000 ) ;
#8814=DIRECTION ( 'NONE',  ( -0.000000000000000000, 1.000000000000000000, -0.000000000000000000 ) ) ;
#8862=ORIENTED_EDGE ( 'NONE', *, *, #59185, .F. ) ;
#9239=EDGE_CURVE ( 'NONE', #7660, #7047, #52645, .T. ) ;
#9305=DIRECTION ( 'NONE',  ( -1.000000000000000000, -0.000000000000000000, -0.000000000000000000 ) ) ;
#10018=ORIENTED_EDGE ( 'NONE', *, *, #1842, .T. ) ;
#10247=LINE ( 'NONE', #57281, #48350 ) ;
#10678=LINE ( 'NONE', #43545, #57737 ) ;
#10922=CARTESIAN_POINT ( 'NONE',  ( 174.0064834503533575, -29.01119750012555443, 5.000000000000000000 ) ) ;
#10960=ORIENTED_EDGE ( 'NONE', *, *, #47939, .T. ) ;
#11593=DIRECTION ( 'NONE',  ( 1.000000000000000000, 0.000000000000000000, -0.000000000000000000 ) ) ;
#11670=ORIENTED_EDGE ( 'NONE', *, *, #66570, .T. ) ;
#11749=STYLED_ITEM ( 'NONE', ( #44306 ), #66405 ) ;
#12116=DIRECTION ( 'NONE',  ( 1.000000000000000000, 0.000000000000000000, 0.000000000000000000 ) ) ;
#12240=DIRECTION ( 'NONE',  ( 1.000000000000000000, 0.000000000000000000, 0.000000000000000000 ) ) ;
#12584=DIRECTION ( 'NONE',  ( 0.000000000000000000, -0.000000000000000000, -1.000000000000000000 ) ) ;
#12642=EDGE_CURVE ( 'NONE', #2475, #14185, #46291, .T. ) ;
#12811=CARTESIAN_POINT ( 'NONE',  ( 152.0064834503532722, 2.160375375128253950, 0.000000000000000000 ) ) ;
#12855=CARTESIAN_POINT ( 'NONE',  ( 152.0064834503532722, 2.160375375128253950, 5.000000000000000000 ) ) ;
#12940=CARTESIAN_POINT ( 'NONE',  ( 154.0064834503532722, -29.01119750012554732, 0.000000000000000000 ) ) ;
#12963=DIRECTION ( 'NONE',  ( 0.000000000000000000, -1.000000000000000000, 0.000000000000000000 ) ) ;
#13087=CARTESIAN_POINT ( 'NONE',  ( 176.0064834503533575, 2.160375375128253950, 0.000000000000000000 ) ) ;
#13437=ORIENTED_EDGE ( 'NONE', *, *, #64224, .F. ) ;
#13450=AXIS2_PLACEMENT_3D ( 'NONE', #33966, #7092, #46674 ) ;
#13625=FACE_OUTER_BOUND ( 'NONE', #59042, .T. ) ;
#13628=CARTESIAN_POINT ( 'NONE',  ( 152.0064834503532722, -35.83962462487175316, 0.000000000000000000 ) ) ;
#13683=AXIS2_PLACEMENT_3D ( 'NONE', #12940, #57489, #61742 ) ;
#13972=MECHANICAL_DESIGN_GEOMETRIC_PRESENTATION_REPRESENTATION('',(#11749),#28655);
#14110=CARTESIAN_POINT ( 'NONE',  ( 176.0064834503533575, -16.00648345035295250, 5.000000000000000000 ) ) ;
#14185=VERTEX_POINT ( 'NONE', #16925 ) ;
#14562=DIRECTION ( 'NONE',  ( 0.000000000000000000, -0.000000000000000000, 1.000000000000000000 ) ) ;
#14875=CARTESIAN_POINT ( 'NONE',  ( 157.4206970127263787, -35.25383818724483831, 0.000000000000000000 ) ) ;
#15473=CARTESIAN_POINT ( 'NONE',  ( 169.1780563256071446, -33.83962462487175316, 0.000000000000000000 ) ) ;
#15746=ADVANCED_FACE ( 'NONE', ( #67438 ), #24291, .F. ) ;
#15882=FACE_OUTER_BOUND ( 'NONE', #24160, .T. ) ;
#15931=CARTESIAN_POINT ( 'NONE',  ( 158.8349105750994568, -33.83962462487175316, 5.000000000000000000 ) ) ;
#15944=DIRECTION ( 'NONE',  ( 1.000000000000000000, 0.000000000000000000, 0.000000000000000000 ) ) ;
#16333=DIRECTION ( 'NONE',  ( -0.000000000000000000, -0.000000000000000000, -1.000000000000000000 ) ) ;
#16441=ORIENTED_EDGE ( 'NONE', *, *, #55038, .F. ) ;
#16768=FILL_AREA_STYLE_COLOUR ( '', #50104 ) ;
#16815=ADVANCED_FACE ( 'NONE', ( #15882 ), #16921, .F. ) ;
#16921=PLANE ( 'NONE',  #39937 ) ;
#16925=CARTESIAN_POINT ( 'NONE',  ( 157.4206970127263787, -35.25383818724481699, 5.000000000000000000 ) ) ;
#17300=AXIS2_PLACEMENT_3D ( 'NONE', #54334, #44382, #17876 ) ;
#17461=VECTOR ( 'NONE', #17463, 1000.000000000000000 ) ;
#17463=DIRECTION ( 'NONE',  ( 0.7071067811865487940, 0.7071067811865463515, -0.000000000000000000 ) ) ;
#17466=( NAMED_UNIT ( * ) SI_UNIT ( $, .STERADIAN. ) SOLID_ANGLE_UNIT ( ) );
#17482=DIRECTION ( 'NONE',  ( 0.7071067811865463515, -0.7071067811865487940, 0.000000000000000000 ) ) ;
#17876=DIRECTION ( 'NONE',  ( 1.000000000000000000, 0.000000000000000000, 0.000000000000000000 ) ) ;
#17939=DIRECTION ( 'NONE',  ( 1.000000000000000000, 0.000000000000000000, 0.000000000000000000 ) ) ;
#18272=DIRECTION ( 'NONE',  ( 0.000000000000000000, -0.000000000000000000, -1.000000000000000000 ) ) ;
#18413=EDGE_CURVE ( 'NONE', #34664, #46063, #4087, .T. ) ;
#18423=ORIENTED_EDGE ( 'NONE', *, *, #1842, .F. ) ;
#18552=VECTOR ( 'NONE', #9305, 1000.000000000000000 ) ;
#19502=CARTESIAN_POINT ( 'NONE',  ( 176.0064834503533575, -29.83962462487173894, 5.000000000000000000 ) ) ;
#19599=FACE_OUTER_BOUND ( 'NONE', #65757, .T. ) ;
#19862=CYLINDRICAL_SURFACE ( 'NONE', #65558, 2.000000000000001776 ) ;
#19909=LINE ( 'NONE', #41481, #18552 ) ;
#20156=EDGE_CURVE ( 'NONE', #22480, #51618, #44623, .T. ) ;
#20478=VECTOR ( 'NONE', #31948, 1000.000000000000000 ) ;
#20691=AXIS2_PLACEMENT_3D ( 'NONE', #46310, #25101, #25814 ) ;
#21143=SHAPE_DEFINITION_REPRESENTATION ( #43085, #53035 ) ;
#21163=CARTESIAN_POINT ( 'NONE',  ( 152.0064834503532722, -29.01119750012554732, 5.000000000000000000 ) ) ;
#21165=CARTESIAN_POINT ( 'NONE',  ( 175.4206970127264356, -30.42541106249864669, 0.000000000000000000 ) ) ;
#21255=LINE ( 'NONE', #37860, #58804 ) ;
#21663=CLOSED_SHELL ( 'NONE', ( #16815, #55988, #49612, #15746, #52033, #56946, #39277, #69776, #40513, #25017, #61315, #47320 ) ) ;
#21969=CARTESIAN_POINT ( 'NONE',  ( 176.0064834503533575, 2.160375375128253950, 5.000000000000000000 ) ) ;
#22402=CARTESIAN_POINT ( 'NONE',  ( 152.0064834503532722, -16.00648345035295250, 0.000000000000000000 ) ) ;
#22480=VERTEX_POINT ( 'NONE', #44970 ) ;
#22583=ORIENTED_EDGE ( 'NONE', *, *, #2579, .F. ) ;
#22754=SURFACE_SIDE_STYLE ('',( #55287 ) ) ;
#22775=CARTESIAN_POINT ( 'NONE',  ( 0.000000000000000000, 0.000000000000000000, 0.000000000000000000 ) ) ;
#22873=ORIENTED_EDGE ( 'NONE', *, *, #66897, .T. ) ;
#23240=CARTESIAN_POINT ( 'NONE',  ( 152.0064834503532722, 2.160375375128253950, 5.000000000000000000 ) ) ;
#24049=DIRECTION ( 'NONE',  ( -0.7071067811865463515, 0.7071067811865487940, -0.000000000000000000 ) ) ;
#24056=EDGE_CURVE ( 'NONE', #69051, #51618, #10247, .T. ) ;
#24117=CIRCLE ( 'NONE', #17300, 2.000000000000001776 ) ;
#24160=EDGE_LOOP ( 'NONE', ( #52558, #26673, #63435, #36763 ) ) ;
#24291=PLANE ( 'NONE',  #24516 ) ;
#24516=AXIS2_PLACEMENT_3D ( 'NONE', #23240, #12963, #18272 ) ;
#24760=CARTESIAN_POINT ( 'NONE',  ( 175.4206970127264356, -30.42541106249864313, 5.000000000000000000 ) ) ;
#24800=CIRCLE ( 'NONE', #33820, 2.000000000000001776 ) ;
#25017=ADVANCED_FACE ( 'NONE', ( #39283 ), #60840, .T. ) ;
#25101=DIRECTION ( 'NONE',  ( -0.000000000000000000, 0.000000000000000000, 1.000000000000000000 ) ) ;
#25180=DIRECTION ( 'NONE',  ( 1.000000000000000000, 0.000000000000000000, 0.000000000000000000 ) ) ;
#25639=LINE ( 'NONE', #4767, #35042 ) ;
#25780=ORIENTED_EDGE ( 'NONE', *, *, #42129, .T. ) ;
#25814=DIRECTION ( 'NONE',  ( 1.000000000000000000, 0.000000000000000000, 0.000000000000000000 ) ) ;
#25823=LINE ( 'NONE', #32164, #37795 ) ;
#26267=ORIENTED_EDGE ( 'NONE', *, *, #20156, .F. ) ;
#26291=ORIENTED_EDGE ( 'NONE', *, *, #30620, .T. ) ;
#26434=LINE ( 'NONE', #42344, #17461 ) ;
#26508=VECTOR ( 'NONE', #24049, 1000.000000000000000 ) ;
#26530=LINE ( 'NONE', #48098, #34221 ) ;
#26600=VECTOR ( 'NONE', #62204, 1000.000000000000000 ) ;
#26673=ORIENTED_EDGE ( 'NONE', *, *, #9239, .T. ) ;
#26814=PRODUCT_DEFINITION_FORMATION_WITH_SPECIFIED_SOURCE ( 'ANY', '', #38037, .NOT_KNOWN. ) ;
#26849=CARTESIAN_POINT ( 'NONE',  ( 152.0064834503532722, -16.00648345035295250, 5.000000000000000000 ) ) ;
#26873=DIRECTION ( 'NONE',  ( -0.000000000000000000, -0.000000000000000000, -1.000000000000000000 ) ) ;
#27028=SURFACE_STYLE_USAGE ( .BOTH. , #22754 ) ;
#27619=VECTOR ( 'NONE', #55813, 1000.000000000000000 ) ;
#27794=AXIS2_PLACEMENT_3D ( 'NONE', #15473, #37042, #58602 ) ;
#28022=ORIENTED_EDGE ( 'NONE', *, *, #18413, .F. ) ;
#28058=DIRECTION ( 'NONE',  ( -0.000000000000000000, 0.000000000000000000, 1.000000000000000000 ) ) ;
#28084=VERTEX_POINT ( 'NONE', #21165 ) ;
#28655=( GEOMETRIC_REPRESENTATION_CONTEXT ( 3 ) GLOBAL_UNCERTAINTY_ASSIGNED_CONTEXT ( ( #54287 ) ) GLOBAL_UNIT_ASSIGNED_CONTEXT ( ( #43281, #37993, #54953 ) ) REPRESENTATION_CONTEXT ( 'NONE', 'WORKASPACE' ) );
#28779=DIRECTION ( 'NONE',  ( 0.000000000000000000, -1.000000000000000000, 0.000000000000000000 ) ) ;
#28834=DIRECTION ( 'NONE',  ( 1.000000000000000000, 3.469446951953611033E-15, 0.000000000000000000 ) ) ;
#29623=LINE ( 'NONE', #61097, #27619 ) ;
#29755=DIRECTION ( 'NONE',  ( 0.000000000000000000, 0.000000000000000000, -1.000000000000000000 ) ) ;
#30058=LINE ( 'NONE', #1787, #26508 ) ;
#30190=EDGE_LOOP ( 'NONE', ( #32275, #8397, #31523, #37997 ) ) ;
#30478=FACE_OUTER_BOUND ( 'NONE', #38333, .T. ) ;
#30620=EDGE_CURVE ( 'NONE', #3378, #67312, #62343, .T. ) ;
#30636=CARTESIAN_POINT ( 'NONE',  ( 152.0064834503532722, 2.160375375128253950, 5.000000000000000000 ) ) ;
#30672=ORIENTED_EDGE ( 'NONE', *, *, #20156, .T. ) ;
#30863=LINE ( 'NONE', #13628, #37973 ) ;
#30875=ORIENTED_EDGE ( 'NONE', *, *, #7672, .T. ) ;
#30933=PRODUCT_DEFINITION ( 'UNKNOWN', '', #26814, #55130 ) ;
#31475=VERTEX_POINT ( 'NONE', #12811 ) ;
#31523=ORIENTED_EDGE ( 'NONE', *, *, #42129, .F. ) ;
#31822=ORIENTED_EDGE ( 'NONE', *, *, #32287, .T. ) ;
#31825=DIRECTION ( 'NONE',  ( -0.000000000000000000, 1.000000000000000000, -0.000000000000000000 ) ) ;
#31870=ORIENTED_EDGE ( 'NONE', *, *, #6716, .F. ) ;
#31948=DIRECTION ( 'NONE',  ( -0.000000000000000000, -0.000000000000000000, 1.000000000000000000 ) ) ;
#31968=DIRECTION ( 'NONE',  ( 0.000000000000000000, -1.000000000000000000, 0.000000000000000000 ) ) ;
#31989=DIRECTION ( 'NONE',  ( 0.000000000000000000, -0.000000000000000000, -1.000000000000000000 ) ) ;
#32164=CARTESIAN_POINT ( 'NONE',  ( 152.5922698879801942, -30.42541106249863603, 0.000000000000000000 ) ) ;
#32275=ORIENTED_EDGE ( 'NONE', *, *, #4285, .T. ) ;
#32287=EDGE_CURVE ( 'NONE', #67312, #69051, #43726, .T. ) ;
#32355=DIRECTION ( 'NONE',  ( 1.000000000000000000, 0.000000000000000000, 0.000000000000000000 ) ) ;
#32618=ORIENTED_EDGE ( 'NONE', *, *, #9239, .F. ) ;
#32923=ORIENTED_EDGE ( 'NONE', *, *, #63401, .F. ) ;
#33043=SHAPE_REPRESENTATION_RELATIONSHIP ( 'NONE' , 'NONE' ,  #53035, #44431 ) ;
#33623=EDGE_CURVE ( 'NONE', #28084, #3378, #29623, .T. ) ;
#33787=VECTOR ( 'NONE', #44737, 1000.000000000000000 ) ;
#33805=EDGE_CURVE ( 'NONE', #43137, #3378, #26434, .T. ) ;
#33820=AXIS2_PLACEMENT_3D ( 'NONE', #56089, #12584, #12240 ) ;
#33966=CARTESIAN_POINT ( 'NONE',  ( 174.0064834503533575, -29.01119750012555443, 5.000000000000000000 ) ) ;
#34087=AXIS2_PLACEMENT_3D ( 'NONE', #61713, #35178, #56757 ) ;
#34221=VECTOR ( 'NONE', #49487, 1000.000000000000000 ) ;
#34296=VECTOR ( 'NONE', #53477, 1000.000000000000000 ) ;
#34376=LINE ( 'NONE', #55970, #34296 ) ;
#34664=VERTEX_POINT ( 'NONE', #54372 ) ;
#34888=AXIS2_PLACEMENT_3D ( 'NONE', #19502, #36115, #29755 ) ;
#34952=ORIENTED_EDGE ( 'NONE', *, *, #63401, .T. ) ;
#35042=VECTOR ( 'NONE', #31989, 1000.000000000000000 ) ;
#35178=DIRECTION ( 'NONE',  ( -0.000000000000000000, 0.000000000000000000, 1.000000000000000000 ) ) ;
#35334=ORIENTED_EDGE ( 'NONE', *, *, #59185, .T. ) ;
#35479=CARTESIAN_POINT ( 'NONE',  ( 152.5922698879801942, -30.42541106249862537, 5.000000000000000000 ) ) ;
#35537=ORIENTED_EDGE ( 'NONE', *, *, #859, .F. ) ;
#36115=DIRECTION ( 'NONE',  ( -0.7071067811865462405, 0.7071067811865487940, 0.000000000000000000 ) ) ;
#36763=ORIENTED_EDGE ( 'NONE', *, *, #859, .T. ) ;
#36942=PLANE ( 'NONE',  #56412 ) ;
#37042=DIRECTION ( 'NONE',  ( 0.000000000000000000, -0.000000000000000000, -1.000000000000000000 ) ) ;
#37258=ORIENTED_EDGE ( 'NONE', *, *, #3572, .T. ) ;
#37502=DIRECTION ( 'NONE',  ( 0.000000000000000000, 0.000000000000000000, -1.000000000000000000 ) ) ;
#37795=VECTOR ( 'NONE', #26873, 1000.000000000000000 ) ;
#37860=CARTESIAN_POINT ( 'NONE',  ( 152.0064834503532722, -35.83962462487175316, 5.000000000000000000 ) ) ;
#37973=VECTOR ( 'NONE', #52438, 1000.000000000000000 ) ;
#37993=( NAMED_UNIT ( * ) PLANE_ANGLE_UNIT ( ) SI_UNIT ( $, .RADIAN. ) );
#37997=ORIENTED_EDGE ( 'NONE', *, *, #41847, .T. ) ;
#38037=PRODUCT ( 'Mounting Feet', 'Mounting Feet', '', ( #58275 ) ) ;
#38112=VECTOR ( 'NONE', #69601, 1000.000000000000000 ) ;
#38280=AXIS2_PLACEMENT_3D ( 'NONE', #64930, #48666, #44372 ) ;
#38333=EDGE_LOOP ( 'NONE', ( #28022, #22583, #65729, #66884 ) ) ;
#38375=CARTESIAN_POINT ( 'NONE',  ( 152.0064834503532722, -29.01119750012554732, 5.000000000000000000 ) ) ;
#38419=CARTESIAN_POINT ( 'NONE',  ( 176.0064834503533575, -29.01119750012555443, 0.000000000000000000 ) ) ;
#38530=ORIENTED_EDGE ( 'NONE', *, *, #66570, .F. ) ;
#39100=ORIENTED_EDGE ( 'NONE', *, *, #18413, .T. ) ;
#39171=PLANE ( 'NONE',  #64615 ) ;
#39277=ADVANCED_FACE ( 'NONE', ( #52043 ), #46032, .F. ) ;
#39283=FACE_OUTER_BOUND ( 'NONE', #8150, .T. ) ;
#39623=CARTESIAN_POINT ( 'NONE',  ( 152.5922698879801942, -30.42541106249863603, 0.000000000000000000 ) ) ;
#39842=DIRECTION ( 'NONE',  ( -0.000000000000000000, 0.000000000000000000, 1.000000000000000000 ) ) ;
#39937=AXIS2_PLACEMENT_3D ( 'NONE', #26849, #11593, #60043 ) ;
#40117=ORIENTED_EDGE ( 'NONE', *, *, #64224, .T. ) ;
#40133=PLANE ( 'NONE',  #34087 ) ;
#40387=DIRECTION ( 'NONE',  ( 0.000000000000000000, -0.000000000000000000, 1.000000000000000000 ) ) ;
#40513=ADVANCED_FACE ( 'NONE', ( #30478 ), #19862, .T. ) ;
#41481=CARTESIAN_POINT ( 'NONE',  ( 152.0064834503532722, 2.160375375128253950, 5.000000000000000000 ) ) ;
#41764=APPLICATION_CONTEXT ( 'automotive_design' ) ;
#41790=AXIS2_PLACEMENT_3D ( 'NONE', #6494, #28058, #49617 ) ;
#41847=EDGE_CURVE ( 'NONE', #48034, #49731, #25639, .T. ) ;
#42129=EDGE_CURVE ( 'NONE', #48034, #4220, #21255, .T. ) ;
#42332=EDGE_CURVE ( 'NONE', #46063, #4220, #65177, .T. ) ;
#42344=CARTESIAN_POINT ( 'NONE',  ( 102.9230540376122462, -102.9230540376126015, 5.000000000000000000 ) ) ;
#42841=ORIENTED_EDGE ( 'NONE', *, *, #32287, .F. ) ;
#43085=PRODUCT_DEFINITION_SHAPE ( 'NONE', 'NONE',  #30933 ) ;
#43137=VERTEX_POINT ( 'NONE', #44105 ) ;
#43281=( LENGTH_UNIT ( ) NAMED_UNIT ( * ) SI_UNIT ( .MILLI., .METRE. ) );
#43545=CARTESIAN_POINT ( 'NONE',  ( 152.0064834503532722, 2.160375375128253950, 5.000000000000000000 ) ) ;
#43674=UNCERTAINTY_MEASURE_WITH_UNIT (LENGTH_MEASURE( 1.000000000000000082E-05 ), #6175, 'distance_accuracy_value', 'NONE');
#43726=LINE ( 'NONE', #38419, #33787 ) ;
#43864=AXIS2_PLACEMENT_3D ( 'NONE', #2547, #40387, #12116 ) ;
#43970=FILL_AREA_STYLE ('',( #16768 ) ) ;
#44072=FACE_OUTER_BOUND ( 'NONE', #47175, .T. ) ;
#44105=CARTESIAN_POINT ( 'NONE',  ( 170.5922698879802510, -35.25383818724482410, 5.000000000000000000 ) ) ;
#44306=PRESENTATION_STYLE_ASSIGNMENT (( #27028 ) ) ;
#44372=DIRECTION ( 'NONE',  ( 1.000000000000000000, 0.000000000000000000, 0.000000000000000000 ) ) ;
#44382=DIRECTION ( 'NONE',  ( -0.000000000000000000, 0.000000000000000000, 1.000000000000000000 ) ) ;
#44431=ADVANCED_BREP_SHAPE_REPRESENTATION ( '', ( #66405, #45918 ), #64023 ) ;
#44623=LINE ( 'NONE', #44983, #8597 ) ;
#44737=DIRECTION ( 'NONE',  ( -0.000000000000000000, 0.000000000000000000, -1.000000000000000000 ) ) ;
#44752=CARTESIAN_POINT ( 'NONE',  ( 158.0064834503532722, -35.83962462487175316, 5.000000000000000000 ) ) ;
#44780=AXIS2_PLACEMENT_3D ( 'NONE', #15931, #37502, #5677 ) ;
#44970=CARTESIAN_POINT ( 'NONE',  ( 176.0064834503533575, 2.160375375128253950, 5.000000000000000000 ) ) ;
#44983=CARTESIAN_POINT ( 'NONE',  ( 176.0064834503533575, 2.160375375128253950, 5.000000000000000000 ) ) ;
#44986=CYLINDRICAL_SURFACE ( 'NONE', #43864, 2.000000000000001776 ) ;
#45652=ORIENTED_EDGE ( 'NONE', *, *, #66083, .T. ) ;
#45918=AXIS2_PLACEMENT_3D ( 'NONE', #22775, #53934, #32355 ) ;
#46032=PLANE ( 'NONE',  #34888 ) ;
#46063=VERTEX_POINT ( 'NONE', #51237 ) ;
#46291=LINE ( 'NONE', #62915, #26600 ) ;
#46310=CARTESIAN_POINT ( 'NONE',  ( 0.000000000000000000, 0.000000000000000000, 0.000000000000000000 ) ) ;
#46674=DIRECTION ( 'NONE',  ( -1.000000000000000000, 0.000000000000000000, 0.000000000000000000 ) ) ;
#46712=ORIENTED_EDGE ( 'NONE', *, *, #33623, .F. ) ;
#46821=DIRECTION ( 'NONE',  ( -1.000000000000000000, 0.000000000000000000, 0.000000000000000000 ) ) ;
#47051=ORIENTED_EDGE ( 'NONE', *, *, #12642, .T. ) ;
#47175=EDGE_LOOP ( 'NONE', ( #4625, #47051, #51029, #37258 ) ) ;
#47256=CARTESIAN_POINT ( 'NONE',  ( 176.0064834503533575, -29.83962462487173894, 0.000000000000000000 ) ) ;
#47320=ADVANCED_FACE ( 'NONE', ( #60562 ), #44986, .T. ) ;
#47561=CARTESIAN_POINT ( 'NONE',  ( 176.0064834503533575, -29.01119750012555087, 5.000000000000000000 ) ) ;
#47662=ORIENTED_EDGE ( 'NONE', *, *, #33805, .T. ) ;
#47939=EDGE_CURVE ( 'NONE', #4220, #43137, #68757, .T. ) ;
#48034=VERTEX_POINT ( 'NONE', #939 ) ;
#48098=CARTESIAN_POINT ( 'NONE',  ( 170.5922698879802226, -35.25383818724483831, 0.000000000000000000 ) ) ;
#48350=VECTOR ( 'NONE', #31825, 1000.000000000000000 ) ;
#48465=EDGE_CURVE ( 'NONE', #7047, #7104, #68903, .T. ) ;
#48666=DIRECTION ( 'NONE',  ( -0.000000000000000000, 0.000000000000000000, 1.000000000000000000 ) ) ;
#48727=CIRCLE ( 'NONE', #13683, 2.000000000000001776 ) ;
#48968=( NAMED_UNIT ( * ) PLANE_ANGLE_UNIT ( ) SI_UNIT ( $, .RADIAN. ) );
#49089=CARTESIAN_POINT ( 'NONE',  ( 152.0064834503532722, -35.83962462487175316, 5.000000000000000000 ) ) ;
#49139=ORIENTED_EDGE ( 'NONE', *, *, #48465, .F. ) ;
#49450=FACE_OUTER_BOUND ( 'NONE', #30190, .T. ) ;
#49487=DIRECTION ( 'NONE',  ( -0.000000000000000000, 0.000000000000000000, -1.000000000000000000 ) ) ;
#49612=ADVANCED_FACE ( 'NONE', ( #19599 ), #36942, .F. ) ;
#49617=DIRECTION ( 'NONE',  ( 1.000000000000000000, 0.000000000000000000, 0.000000000000000000 ) ) ;
#49731=VERTEX_POINT ( 'NONE', #60136 ) ;
#50104=COLOUR_RGB ( '', 0.40784314, 0.44705882, 0.49803922) ;
#50120=DIRECTION ( 'NONE',  ( 0.000000000000000000, 1.000000000000000000, 0.000000000000000000 ) ) ;
#50250=ORIENTED_EDGE ( 'NONE', *, *, #3572, .F. ) ;
#51029=ORIENTED_EDGE ( 'NONE', *, *, #7025, .F. ) ;
#51237=CARTESIAN_POINT ( 'NONE',  ( 169.1780563256071446, -35.83962462487175316, 0.000000000000000000 ) ) ;
#51385=ORIENTED_EDGE ( 'NONE', *, *, #33805, .F. ) ;
#51618=VERTEX_POINT ( 'NONE', #13087 ) ;
#52033=ADVANCED_FACE ( 'NONE', ( #13625 ), #40133, .T. ) ;
#52043=FACE_OUTER_BOUND ( 'NONE', #1484, .T. ) ;
#52053=CARTESIAN_POINT ( 'NONE',  ( 169.1780563256071446, -33.83962462487175316, 5.000000000000000000 ) ) ;
#52327=PLANE ( 'NONE',  #20691 ) ;
#52438=DIRECTION ( 'NONE',  ( 1.000000000000000000, 0.000000000000000000, 0.000000000000000000 ) ) ;
#52558=ORIENTED_EDGE ( 'NONE', *, *, #55038, .T. ) ;
#52645=LINE ( 'NONE', #21163, #38112 ) ;
#53035=SHAPE_REPRESENTATION ( 'Mounting Feet', ( #45918 ), #64023 ) ;
#53477=DIRECTION ( 'NONE',  ( -1.000000000000000000, -0.000000000000000000, -0.000000000000000000 ) ) ;
#53934=DIRECTION ( 'NONE',  ( 0.000000000000000000, 0.000000000000000000, 1.000000000000000000 ) ) ;
#54287=UNCERTAINTY_MEASURE_WITH_UNIT (LENGTH_MEASURE( 1.000000000000000082E-05 ), #43281, 'distance_accuracy_value', 'NONE');
#54334=CARTESIAN_POINT ( 'NONE',  ( 158.8349105750994568, -33.83962462487175316, 5.000000000000000000 ) ) ;
#54372=CARTESIAN_POINT ( 'NONE',  ( 170.5922698879802226, -35.25383818724483831, 0.000000000000000000 ) ) ;
#54747=DIRECTION ( 'NONE',  ( 0.000000000000000000, -0.000000000000000000, 1.000000000000000000 ) ) ;
#54920=ORIENTED_EDGE ( 'NONE', *, *, #7672, .F. ) ;
#54953=( NAMED_UNIT ( * ) SI_UNIT ( $, .STERADIAN. ) SOLID_ANGLE_UNIT ( ) );
#55038=EDGE_CURVE ( 'NONE', #31475, #7660, #5795, .T. ) ;
#55130=PRODUCT_DEFINITION_CONTEXT ( 'detailed design', #41764, 'design' ) ;
#55287=SURFACE_STYLE_FILL_AREA ( #43970 ) ;
#55386=CARTESIAN_POINT ( 'NONE',  ( 158.8349105750994568, -33.83962462487175316, 0.000000000000000000 ) ) ;
#55389=PLANE ( 'NONE',  #65229 ) ;
#55813=DIRECTION ( 'NONE',  ( -0.000000000000000000, -0.000000000000000000, 1.000000000000000000 ) ) ;
#55970=CARTESIAN_POINT ( 'NONE',  ( 152.0064834503532722, 2.160375375128253950, 0.000000000000000000 ) ) ;
#55988=ADVANCED_FACE ( 'NONE', ( #49450 ), #39171, .F. ) ;
#56072=CARTESIAN_POINT ( 'NONE',  ( 169.1780563256071446, -35.83962462487175316, 5.000000000000000000 ) ) ;
#56089=CARTESIAN_POINT ( 'NONE',  ( 174.0064834503533575, -29.01119750012555443, 0.000000000000000000 ) ) ;
#56412=AXIS2_PLACEMENT_3D ( 'NONE', #21969, #46821, #63449 ) ;
#56757=DIRECTION ( 'NONE',  ( 1.000000000000000000, 0.000000000000000000, 0.000000000000000000 ) ) ;
#56946=ADVANCED_FACE ( 'NONE', ( #2825 ), #52327, .F. ) ;
#57115=EDGE_LOOP ( 'NONE', ( #31870, #50250, #49139, #32618 ) ) ;
#57281=CARTESIAN_POINT ( 'NONE',  ( 176.0064834503533575, 2.160375375128253950, 0.000000000000000000 ) ) ;
#57446=ORIENTED_EDGE ( 'NONE', *, *, #12642, .F. ) ;
#57489=DIRECTION ( 'NONE',  ( 0.000000000000000000, -0.000000000000000000, -1.000000000000000000 ) ) ;
#57651=ORIENTED_EDGE ( 'NONE', *, *, #66083, .F. ) ;
#57737=VECTOR ( 'NONE', #16333, 1000.000000000000000 ) ;
#58275=PRODUCT_CONTEXT ( 'NONE', #66133, 'mechanical' ) ;
#58602=DIRECTION ( 'NONE',  ( 1.000000000000000000, 6.938893903907222067E-15, 0.000000000000000000 ) ) ;
#58796=ORIENTED_EDGE ( 'NONE', *, *, #6716, .T. ) ;
#58804=VECTOR ( 'NONE', #15944, 1000.000000000000000 ) ;
#59042=EDGE_LOOP ( 'NONE', ( #25780, #10960, #47662, #26291, #40117, #35334, #68897, #62505, #791, #45652 ) ) ;
#59185=EDGE_CURVE ( 'NONE', #22480, #63319, #19909, .T. ) ;
#59199=ORIENTED_EDGE ( 'NONE', *, *, #24056, .F. ) ;
#60043=DIRECTION ( 'NONE',  ( -0.000000000000000000, 0.000000000000000000, -1.000000000000000000 ) ) ;
#60093=CYLINDRICAL_SURFACE ( 'NONE', #44780, 2.000000000000001776 ) ;
#60136=CARTESIAN_POINT ( 'NONE',  ( 158.8349105750994568, -35.83962462487175316, 0.000000000000000000 ) ) ;
#60497=EDGE_LOOP ( 'NONE', ( #11670, #35537, #8862, #30672 ) ) ;
#60562=FACE_OUTER_BOUND ( 'NONE', #57115, .T. ) ;
#60840=CYLINDRICAL_SURFACE ( 'NONE', #13450, 2.000000000000001776 ) ;
#61026=CARTESIAN_POINT ( 'NONE',  ( 152.0064834503532722, -29.01119750012554377, 0.000000000000000000 ) ) ;
#61097=CARTESIAN_POINT ( 'NONE',  ( 175.4206970127264356, -30.42541106249864669, 5.000000000000000000 ) ) ;
#61315=ADVANCED_FACE ( 'NONE', ( #25 ), #60093, .T. ) ;
#61713=CARTESIAN_POINT ( 'NONE',  ( 0.000000000000000000, 0.000000000000000000, 5.000000000000000000 ) ) ;
#61742=DIRECTION ( 'NONE',  ( 1.000000000000000000, -8.673617379884027583E-15, 0.000000000000000000 ) ) ;
#62204=DIRECTION ( 'NONE',  ( -0.000000000000000000, -0.000000000000000000, 1.000000000000000000 ) ) ;
#62289=VECTOR ( 'NONE', #28779, 1000.000000000000000 ) ;
#62343=CIRCLE ( 'NONE', #5886, 2.000000000000001776 ) ;
#62439=DIRECTION ( 'NONE',  ( -0.7071067811865487940, -0.7071067811865463515, -0.000000000000000000 ) ) ;
#62505=ORIENTED_EDGE ( 'NONE', *, *, #48465, .T. ) ;
#62774=DIRECTION ( 'NONE',  ( -0.000000000000000000, 0.000000000000000000, -1.000000000000000000 ) ) ;
#62915=CARTESIAN_POINT ( 'NONE',  ( 157.4206970127263787, -35.25383818724483831, 5.000000000000000000 ) ) ;
#63319=VERTEX_POINT ( 'NONE', #30636 ) ;
#63399=CIRCLE ( 'NONE', #2401, 2.000000000000001776 ) ;
#63401=EDGE_CURVE ( 'NONE', #28084, #34664, #2699, .T. ) ;
#63435=ORIENTED_EDGE ( 'NONE', *, *, #7185, .F. ) ;
#63449=DIRECTION ( 'NONE',  ( 0.000000000000000000, 0.000000000000000000, 1.000000000000000000 ) ) ;
#63781=EDGE_LOOP ( 'NONE', ( #34952, #39100, #64143, #10018, #22873, #58796, #16441, #38530, #59199, #30875 ) ) ;
#64023=( GEOMETRIC_REPRESENTATION_CONTEXT ( 3 ) GLOBAL_UNCERTAINTY_ASSIGNED_CONTEXT ( ( #43674 ) ) GLOBAL_UNIT_ASSIGNED_CONTEXT ( ( #6175, #48968, #17466 ) ) REPRESENTATION_CONTEXT ( 'NONE', 'WORKASPACE' ) );
#64143=ORIENTED_EDGE ( 'NONE', *, *, #4285, .F. ) ;
#64224=EDGE_CURVE ( 'NONE', #67312, #22480, #68915, .T. ) ;
#64527=VECTOR ( 'NONE', #31968, 1000.000000000000000 ) ;
#64615=AXIS2_PLACEMENT_3D ( 'NONE', #49089, #50120, #54747 ) ;
#64930=CARTESIAN_POINT ( 'NONE',  ( 169.1780563256071446, -33.83962462487175316, 5.000000000000000000 ) ) ;
#65177=LINE ( 'NONE', #5073, #20478 ) ;
#65229=AXIS2_PLACEMENT_3D ( 'NONE', #44752, #6929, #62774 ) ;
#65558=AXIS2_PLACEMENT_3D ( 'NONE', #52053, #14562, #25180 ) ;
#65729=ORIENTED_EDGE ( 'NONE', *, *, #47939, .F. ) ;
#65757=EDGE_LOOP ( 'NONE', ( #13437, #31822, #4864, #26267 ) ) ;
#66083=EDGE_CURVE ( 'NONE', #14185, #48034, #24117, .T. ) ;
#66092=ORIENTED_EDGE ( 'NONE', *, *, #2579, .T. ) ;
#66133=APPLICATION_CONTEXT ( 'automotive_design' ) ;
#66282=LINE ( 'NONE', #6191, #1327 ) ;
#66405=MANIFOLD_SOLID_BREP ( 'Fillet1', #21663 ) ;
#66554=DIRECTION ( 'NONE',  ( -0.000000000000000000, -0.000000000000000000, -1.000000000000000000 ) ) ;
#66570=EDGE_CURVE ( 'NONE', #51618, #31475, #34376, .T. ) ;
#66884=ORIENTED_EDGE ( 'NONE', *, *, #42332, .F. ) ;
#66897=EDGE_CURVE ( 'NONE', #2475, #67892, #30058, .T. ) ;
#67171=EDGE_LOOP ( 'NONE', ( #57651, #57446, #18423, #67539 ) ) ;
#67312=VERTEX_POINT ( 'NONE', #47561 ) ;
#67438=FACE_OUTER_BOUND ( 'NONE', #60497, .T. ) ;
#67539=ORIENTED_EDGE ( 'NONE', *, *, #41847, .F. ) ;
#67892=VERTEX_POINT ( 'NONE', #39623 ) ;
#68757=CIRCLE ( 'NONE', #38280, 2.000000000000001776 ) ;
#68897=ORIENTED_EDGE ( 'NONE', *, *, #7185, .T. ) ;
#68903=CIRCLE ( 'NONE', #41790, 2.000000000000001776 ) ;
#68915=LINE ( 'NONE', #14110, #2573 ) ;
#69051=VERTEX_POINT ( 'NONE', #4271 ) ;
#69601=DIRECTION ( 'NONE',  ( 0.000000000000000000, -0.000000000000000000, 1.000000000000000000 ) ) ;
#69776=ADVANCED_FACE ( 'NONE', ( #44072 ), #55389, .F. ) ;
#69891=ORIENTED_EDGE ( 'NONE', *, *, #33623, .T. ) ;
ENDSEC;
END-ISO-10303-21;
